ISO-10303-21;
HEADER;
/* Generated by software containing ST-Developer
 * from STEP Tools, Inc. (www.steptools.com) 
 */

FILE_DESCRIPTION(
/* description */ ('Five-roller gravity conveyor'),
/* implementation_level */ '2;1');

FILE_NAME(
/* name */ 'Slot nut.step',
/* time_stamp */ '2026-10-29T15:36:43-07:00',
/* author */ (''),
/* organization */ (''),
/* preprocessor_version */ 'ST-DEVELOPER v20.2',
/* originating_system */ 'Autodesk Translation Framework v15.17.0.0',
/* authorisation */ '');

FILE_SCHEMA (('AUTOMOTIVE_DESIGN { 1 0 10303 214 3 1 1 }'));
ENDSEC;

DATA;
#10=MECHANICAL_DESIGN_GEOMETRIC_PRESENTATION_REPRESENTATION('',(#317),#7806);
#259=ELLIPSE('',#4608,0.299389011154384,0.2117);
#260=ELLIPSE('',#4612,0.299389011154384,0.2117);
#281=SHAPE_REPRESENTATION_RELATIONSHIP('SRR','None',#7918,#299);
#299=ADVANCED_BREP_SHAPE_REPRESENTATION('',(#342),#7791);
#317=STYLED_ITEM('',(#8098),#342);
#342=MANIFOLD_SOLID_BREP('Body1',#4205);
#381=FACE_BOUND('',#1022,.T.);
#468=CIRCLE('',#4601,0.2117);
#469=CIRCLE('',#4610,0.2117);
#470=CIRCLE('',#4611,0.2117);
#471=CIRCLE('',#4613,0.2117);
#616=CYLINDRICAL_SURFACE('',#4609,0.2117);
#768=FACE_OUTER_BOUND('',#1019,.T.);
#769=FACE_OUTER_BOUND('',#1020,.T.);
#770=FACE_OUTER_BOUND('',#1021,.T.);
#771=FACE_OUTER_BOUND('',#1023,.T.);
#772=FACE_OUTER_BOUND('',#1024,.T.);
#773=FACE_OUTER_BOUND('',#1025,.T.);
#774=FACE_OUTER_BOUND('',#1026,.T.);
#775=FACE_OUTER_BOUND('',#1027,.T.);
#776=FACE_OUTER_BOUND('',#1028,.T.);
#777=FACE_OUTER_BOUND('',#1029,.T.);
#778=FACE_OUTER_BOUND('',#1030,.T.);
#779=FACE_OUTER_BOUND('',#1031,.T.);
#780=FACE_OUTER_BOUND('',#1032,.T.);
#781=FACE_OUTER_BOUND('',#1033,.T.);
#1019=EDGE_LOOP('',(#3342,#3343,#3344,#3345));
#1020=EDGE_LOOP('',(#3346,#3347,#3348,#3349));
#1021=EDGE_LOOP('',(#3350,#3351,#3352,#3353));
#1022=EDGE_LOOP('',(#3354));
#1023=EDGE_LOOP('',(#3355,#3356,#3357,#3358,#3359,#3360,#3361,#3362,#3363,
#3364));
#1024=EDGE_LOOP('',(#3365,#3366,#3367,#3368));
#1025=EDGE_LOOP('',(#3369,#3370,#3371,#3372));
#1026=EDGE_LOOP('',(#3373,#3374,#3375,#3376,#3377,#3378,#3379,#3380,#3381,
#3382));
#1027=EDGE_LOOP('',(#3383,#3384,#3385,#3386));
#1028=EDGE_LOOP('',(#3387,#3388,#3389,#3390,#3391,#3392));
#1029=EDGE_LOOP('',(#3393,#3394,#3395,#3396,#3397,#3398,#3399,#3400));
#1030=EDGE_LOOP('',(#3401,#3402,#3403,#3404,#3405));
#1031=EDGE_LOOP('',(#3406,#3407,#3408,#3409));
#1032=EDGE_LOOP('',(#3410,#3411,#3412,#3413,#3414,#3415));
#1033=EDGE_LOOP('',(#3416,#3417,#3418,#3419));
#1422=LINE('',#6833,#1763);
#1423=LINE('',#6835,#1764);
#1424=LINE('',#6837,#1765);
#1425=LINE('',#6838,#1766);
#1426=LINE('',#6841,#1767);
#1427=LINE('',#6843,#1768);
#1428=LINE('',#6844,#1769);
#1429=LINE('',#6847,#1770);
#1430=LINE('',#6849,#1771);
#1431=LINE('',#6850,#1772);
#1432=LINE('',#6855,#1773);
#1433=LINE('',#6857,#1774);
#1434=LINE('',#6859,#1775);
#1435=LINE('',#6861,#1776);
#1436=LINE('',#6863,#1777);
#1437=LINE('',#6865,#1778);
#1438=LINE('',#6866,#1779);
#1439=LINE('',#6869,#1780);
#1440=LINE('',#6870,#1781);
#1441=LINE('',#6873,#1782);
#1442=LINE('',#6874,#1783);
#1443=LINE('',#6877,#1784);
#1444=LINE('',#6879,#1785);
#1445=LINE('',#6881,#1786);
#1446=LINE('',#6883,#1787);
#1447=LINE('',#6884,#1788);
#1448=LINE('',#6886,#1789);
#1449=LINE('',#6889,#1790);
#1450=LINE('',#6892,#1791);
#1451=LINE('',#6896,#1792);
#1452=LINE('',#6903,#1793);
#1453=LINE('',#6905,#1794);
#1454=LINE('',#6907,#1795);
#1763=VECTOR('',#5502,1.);
#1764=VECTOR('',#5503,1.);
#1765=VECTOR('',#5504,1.);
#1766=VECTOR('',#5505,1.);
#1767=VECTOR('',#5508,1.);
#1768=VECTOR('',#5509,1.);
#1769=VECTOR('',#5510,1.);
#1770=VECTOR('',#5513,1.);
#1771=VECTOR('',#5514,1.);
#1772=VECTOR('',#5515,1.);
#1773=VECTOR('',#5520,1.);
#1774=VECTOR('',#5521,1.);
#1775=VECTOR('',#5522,1.);
#1776=VECTOR('',#5523,1.);
#1777=VECTOR('',#5524,1.);
#1778=VECTOR('',#5525,1.);
#1779=VECTOR('',#5526,1.);
#1780=VECTOR('',#5529,1.);
#1781=VECTOR('',#5530,1.);
#1782=VECTOR('',#5533,1.);
#1783=VECTOR('',#5534,1.);
#1784=VECTOR('',#5537,1.);
#1785=VECTOR('',#5538,1.);
#1786=VECTOR('',#5539,1.);
#1787=VECTOR('',#5540,1.);
#1788=VECTOR('',#5541,1.);
#1789=VECTOR('',#5544,1.);
#1790=VECTOR('',#5547,1.);
#1791=VECTOR('',#5550,1.);
#1792=VECTOR('',#5555,0.21);
#1793=VECTOR('',#5564,1.);
#1794=VECTOR('',#5567,1.);
#1795=VECTOR('',#5570,1.);
#2052=VERTEX_POINT('',#6831);
#2053=VERTEX_POINT('',#6832);
#2054=VERTEX_POINT('',#6834);
#2055=VERTEX_POINT('',#6836);
#2056=VERTEX_POINT('',#6840);
#2057=VERTEX_POINT('',#6842);
#2058=VERTEX_POINT('',#6846);
#2059=VERTEX_POINT('',#6848);
#2060=VERTEX_POINT('',#6851);
#2061=VERTEX_POINT('',#6854);
#2062=VERTEX_POINT('',#6856);
#2063=VERTEX_POINT('',#6858);
#2064=VERTEX_POINT('',#6860);
#2065=VERTEX_POINT('',#6862);
#2066=VERTEX_POINT('',#6864);
#2067=VERTEX_POINT('',#6868);
#2068=VERTEX_POINT('',#6872);
#2069=VERTEX_POINT('',#6876);
#2070=VERTEX_POINT('',#6878);
#2071=VERTEX_POINT('',#6880);
#2072=VERTEX_POINT('',#6882);
#2073=VERTEX_POINT('',#6888);
#2074=VERTEX_POINT('',#6890);
#2075=VERTEX_POINT('',#6894);
#2076=VERTEX_POINT('',#6897);
#2077=VERTEX_POINT('',#6899);
#2514=EDGE_CURVE('',#2052,#2053,#1422,.T.);
#2515=EDGE_CURVE('',#2054,#2052,#1423,.T.);
#2516=EDGE_CURVE('',#2055,#2054,#1424,.T.);
#2517=EDGE_CURVE('',#2053,#2055,#1425,.T.);
#2518=EDGE_CURVE('',#2054,#2056,#1426,.T.);
#2519=EDGE_CURVE('',#2057,#2056,#1427,.T.);
#2520=EDGE_CURVE('',#2055,#2057,#1428,.T.);
#2521=EDGE_CURVE('',#2056,#2058,#1429,.T.);
#2522=EDGE_CURVE('',#2058,#2059,#1430,.T.);
#2523=EDGE_CURVE('',#2059,#2057,#1431,.T.);
#2524=EDGE_CURVE('',#2060,#2060,#468,.T.);
#2525=EDGE_CURVE('',#2061,#2052,#1432,.T.);
#2526=EDGE_CURVE('',#2062,#2061,#1433,.T.);
#2527=EDGE_CURVE('',#2062,#2063,#1434,.T.);
#2528=EDGE_CURVE('',#2064,#2063,#1435,.T.);
#2529=EDGE_CURVE('',#2064,#2065,#1436,.T.);
#2530=EDGE_CURVE('',#2065,#2066,#1437,.T.);
#2531=EDGE_CURVE('',#2066,#2058,#1438,.T.);
#2532=EDGE_CURVE('',#2066,#2067,#1439,.T.);
#2533=EDGE_CURVE('',#2067,#2059,#1440,.T.);
#2534=EDGE_CURVE('',#2068,#2065,#1441,.T.);
#2535=EDGE_CURVE('',#2067,#2068,#1442,.T.);
#2536=EDGE_CURVE('',#2069,#2068,#1443,.T.);
#2537=EDGE_CURVE('',#2070,#2069,#1444,.T.);
#2538=EDGE_CURVE('',#2070,#2071,#1445,.T.);
#2539=EDGE_CURVE('',#2072,#2071,#1446,.T.);
#2540=EDGE_CURVE('',#2072,#2053,#1447,.T.);
#2541=EDGE_CURVE('',#2069,#2064,#1448,.T.);
#2542=EDGE_CURVE('',#2063,#2073,#1449,.T.);
#2543=EDGE_CURVE('',#2073,#2074,#259,.T.);
#2544=EDGE_CURVE('',#2074,#2070,#1450,.T.);
#2545=EDGE_CURVE('',#2075,#2073,#469,.F.);
#2546=EDGE_CURVE('',#2075,#2060,#1451,.T.);
#2547=EDGE_CURVE('',#2076,#2075,#470,.F.);
#2548=EDGE_CURVE('',#2077,#2076,#260,.T.);
#2549=EDGE_CURVE('',#2074,#2077,#471,.F.);
#2550=EDGE_CURVE('',#2076,#2062,#1452,.T.);
#2551=EDGE_CURVE('',#2071,#2077,#1453,.T.);
#2552=EDGE_CURVE('',#2061,#2072,#1454,.T.);
#3342=ORIENTED_EDGE('',*,*,#2514,.F.);
#3343=ORIENTED_EDGE('',*,*,#2515,.F.);
#3344=ORIENTED_EDGE('',*,*,#2516,.F.);
#3345=ORIENTED_EDGE('',*,*,#2517,.F.);
#3346=ORIENTED_EDGE('',*,*,#2516,.T.);
#3347=ORIENTED_EDGE('',*,*,#2518,.T.);
#3348=ORIENTED_EDGE('',*,*,#2519,.F.);
#3349=ORIENTED_EDGE('',*,*,#2520,.F.);
#3350=ORIENTED_EDGE('',*,*,#2521,.T.);
#3351=ORIENTED_EDGE('',*,*,#2522,.T.);
#3352=ORIENTED_EDGE('',*,*,#2523,.T.);
#3353=ORIENTED_EDGE('',*,*,#2519,.T.);
#3354=ORIENTED_EDGE('',*,*,#2524,.T.);
#3355=ORIENTED_EDGE('',*,*,#2521,.F.);
#3356=ORIENTED_EDGE('',*,*,#2518,.F.);
#3357=ORIENTED_EDGE('',*,*,#2515,.T.);
#3358=ORIENTED_EDGE('',*,*,#2525,.F.);
#3359=ORIENTED_EDGE('',*,*,#2526,.F.);
#3360=ORIENTED_EDGE('',*,*,#2527,.T.);
#3361=ORIENTED_EDGE('',*,*,#2528,.F.);
#3362=ORIENTED_EDGE('',*,*,#2529,.T.);
#3363=ORIENTED_EDGE('',*,*,#2530,.T.);
#3364=ORIENTED_EDGE('',*,*,#2531,.T.);
#3365=ORIENTED_EDGE('',*,*,#2532,.T.);
#3366=ORIENTED_EDGE('',*,*,#2533,.T.);
#3367=ORIENTED_EDGE('',*,*,#2522,.F.);
#3368=ORIENTED_EDGE('',*,*,#2531,.F.);
#3369=ORIENTED_EDGE('',*,*,#2534,.F.);
#3370=ORIENTED_EDGE('',*,*,#2535,.F.);
#3371=ORIENTED_EDGE('',*,*,#2532,.F.);
#3372=ORIENTED_EDGE('',*,*,#2530,.F.);
#3373=ORIENTED_EDGE('',*,*,#2523,.F.);
#3374=ORIENTED_EDGE('',*,*,#2533,.F.);
#3375=ORIENTED_EDGE('',*,*,#2535,.T.);
#3376=ORIENTED_EDGE('',*,*,#2536,.F.);
#3377=ORIENTED_EDGE('',*,*,#2537,.F.);
#3378=ORIENTED_EDGE('',*,*,#2538,.T.);
#3379=ORIENTED_EDGE('',*,*,#2539,.F.);
#3380=ORIENTED_EDGE('',*,*,#2540,.T.);
#3381=ORIENTED_EDGE('',*,*,#2517,.T.);
#3382=ORIENTED_EDGE('',*,*,#2520,.T.);
#3383=ORIENTED_EDGE('',*,*,#2534,.T.);
#3384=ORIENTED_EDGE('',*,*,#2529,.F.);
#3385=ORIENTED_EDGE('',*,*,#2541,.F.);
#3386=ORIENTED_EDGE('',*,*,#2536,.T.);
#3387=ORIENTED_EDGE('',*,*,#2537,.T.);
#3388=ORIENTED_EDGE('',*,*,#2541,.T.);
#3389=ORIENTED_EDGE('',*,*,#2528,.T.);
#3390=ORIENTED_EDGE('',*,*,#2542,.T.);
#3391=ORIENTED_EDGE('',*,*,#2543,.T.);
#3392=ORIENTED_EDGE('',*,*,#2544,.T.);
#3393=ORIENTED_EDGE('',*,*,#2543,.F.);
#3394=ORIENTED_EDGE('',*,*,#2545,.F.);
#3395=ORIENTED_EDGE('',*,*,#2546,.T.);
#3396=ORIENTED_EDGE('',*,*,#2524,.F.);
#3397=ORIENTED_EDGE('',*,*,#2546,.F.);
#3398=ORIENTED_EDGE('',*,*,#2547,.F.);
#3399=ORIENTED_EDGE('',*,*,#2548,.F.);
#3400=ORIENTED_EDGE('',*,*,#2549,.F.);
#3401=ORIENTED_EDGE('',*,*,#2542,.F.);
#3402=ORIENTED_EDGE('',*,*,#2527,.F.);
#3403=ORIENTED_EDGE('',*,*,#2550,.F.);
#3404=ORIENTED_EDGE('',*,*,#2547,.T.);
#3405=ORIENTED_EDGE('',*,*,#2545,.T.);
#3406=ORIENTED_EDGE('',*,*,#2544,.F.);
#3407=ORIENTED_EDGE('',*,*,#2549,.T.);
#3408=ORIENTED_EDGE('',*,*,#2551,.F.);
#3409=ORIENTED_EDGE('',*,*,#2538,.F.);
#3410=ORIENTED_EDGE('',*,*,#2526,.T.);
#3411=ORIENTED_EDGE('',*,*,#2552,.T.);
#3412=ORIENTED_EDGE('',*,*,#2539,.T.);
#3413=ORIENTED_EDGE('',*,*,#2551,.T.);
#3414=ORIENTED_EDGE('',*,*,#2548,.T.);
#3415=ORIENTED_EDGE('',*,*,#2550,.T.);
#3416=ORIENTED_EDGE('',*,*,#2514,.T.);
#3417=ORIENTED_EDGE('',*,*,#2540,.F.);
#3418=ORIENTED_EDGE('',*,*,#2552,.F.);
#3419=ORIENTED_EDGE('',*,*,#2525,.T.);
#3913=PLANE('',#4598);
#3914=PLANE('',#4599);
#3915=PLANE('',#4600);
#3916=PLANE('',#4602);
#3917=PLANE('',#4603);
#3918=PLANE('',#4604);
#3919=PLANE('',#4605);
#3920=PLANE('',#4606);
#3921=PLANE('',#4607);
#3922=PLANE('',#4614);
#3923=PLANE('',#4615);
#3924=PLANE('',#4616);
#3925=PLANE('',#4617);
#4083=ADVANCED_FACE('',(#768),#3913,.F.);
#4084=ADVANCED_FACE('',(#769),#3914,.T.);
#4085=ADVANCED_FACE('',(#770,#381),#3915,.T.);
#4086=ADVANCED_FACE('',(#771),#3916,.T.);
#4087=ADVANCED_FACE('',(#772),#3917,.T.);
#4088=ADVANCED_FACE('',(#773),#3918,.F.);
#4089=ADVANCED_FACE('',(#774),#3919,.T.);
#4090=ADVANCED_FACE('',(#775),#3920,.T.);
#4091=ADVANCED_FACE('',(#776),#3921,.T.);
#4092=ADVANCED_FACE('',(#777),#616,.F.);
#4093=ADVANCED_FACE('',(#778),#3922,.F.);
#4094=ADVANCED_FACE('',(#779),#3923,.F.);
#4095=ADVANCED_FACE('',(#780),#3924,.T.);
#4096=ADVANCED_FACE('',(#781),#3925,.T.);
#4205=CLOSED_SHELL('',(#4083,#4084,#4085,#4086,#4087,#4088,#4089,#4090,
#4091,#4092,#4093,#4094,#4095,#4096));
#4597=AXIS2_PLACEMENT_3D('',#6829,#5498,#5499);
#4598=AXIS2_PLACEMENT_3D('',#6830,#5500,#5501);
#4599=AXIS2_PLACEMENT_3D('',#6839,#5506,#5507);
#4600=AXIS2_PLACEMENT_3D('',#6845,#5511,#5512);
#4601=AXIS2_PLACEMENT_3D('',#6852,#5516,#5517);
#4602=AXIS2_PLACEMENT_3D('',#6853,#5518,#5519);
#4603=AXIS2_PLACEMENT_3D('',#6867,#5527,#5528);
#4604=AXIS2_PLACEMENT_3D('',#6871,#5531,#5532);
#4605=AXIS2_PLACEMENT_3D('',#6875,#5535,#5536);
#4606=AXIS2_PLACEMENT_3D('',#6885,#5542,#5543);
#4607=AXIS2_PLACEMENT_3D('',#6887,#5545,#5546);
#4608=AXIS2_PLACEMENT_3D('',#6891,#5548,#5549);
#4609=AXIS2_PLACEMENT_3D('',#6893,#5551,#5552);
#4610=AXIS2_PLACEMENT_3D('',#6895,#5553,#5554);
#4611=AXIS2_PLACEMENT_3D('',#6898,#5556,#5557);
#4612=AXIS2_PLACEMENT_3D('',#6900,#5558,#5559);
#4613=AXIS2_PLACEMENT_3D('',#6901,#5560,#5561);
#4614=AXIS2_PLACEMENT_3D('',#6902,#5562,#5563);
#4615=AXIS2_PLACEMENT_3D('',#6904,#5565,#5566);
#4616=AXIS2_PLACEMENT_3D('',#6906,#5568,#5569);
#4617=AXIS2_PLACEMENT_3D('',#6908,#5571,#5572);
#5498=DIRECTION('axis',(0.,0.,1.));
#5499=DIRECTION('refdir',(1.,0.,0.));
#5500=DIRECTION('center_axis',(0.,0.,1.));
#5501=DIRECTION('ref_axis',(1.,0.,0.));
#5502=DIRECTION('',(1.,0.,0.));
#5503=DIRECTION('',(0.,-1.,0.));
#5504=DIRECTION('',(-1.,0.,0.));
#5505=DIRECTION('',(0.,1.,0.));
#5506=DIRECTION('center_axis',(0.,1.,0.));
#5507=DIRECTION('ref_axis',(-1.,0.,0.));
#5508=DIRECTION('',(0.,0.,1.));
#5509=DIRECTION('',(-1.,0.,0.));
#5510=DIRECTION('',(0.,0.,1.));
#5511=DIRECTION('center_axis',(0.,0.,1.));
#5512=DIRECTION('ref_axis',(1.,0.,0.));
#5513=DIRECTION('',(0.,-1.,0.));
#5514=DIRECTION('',(1.,0.,0.));
#5515=DIRECTION('',(0.,1.,0.));
#5516=DIRECTION('center_axis',(0.,0.,-1.));
#5517=DIRECTION('ref_axis',(1.,0.,0.));
#5518=DIRECTION('center_axis',(-1.,0.,0.));
#5519=DIRECTION('ref_axis',(0.,-1.,0.));
#5520=DIRECTION('',(0.,0.,1.));
#5521=DIRECTION('',(0.,0.707106781186548,0.707106781186548));
#5522=DIRECTION('',(0.,-1.,0.));
#5523=DIRECTION('',(0.,0.707106781186548,-0.707106781186548));
#5524=DIRECTION('',(0.,0.,1.));
#5525=DIRECTION('',(0.,-1.,0.));
#5526=DIRECTION('',(0.,0.,1.));
#5527=DIRECTION('center_axis',(0.,-1.,0.));
#5528=DIRECTION('ref_axis',(1.,0.,0.));
#5529=DIRECTION('',(1.,0.,0.));
#5530=DIRECTION('',(0.,0.,1.));
#5531=DIRECTION('center_axis',(0.,0.,1.));
#5532=DIRECTION('ref_axis',(1.,0.,0.));
#5533=DIRECTION('',(-1.,0.,0.));
#5534=DIRECTION('',(0.,1.,0.));
#5535=DIRECTION('center_axis',(1.,0.,0.));
#5536=DIRECTION('ref_axis',(0.,1.,0.));
#5537=DIRECTION('',(0.,0.,1.));
#5538=DIRECTION('',(0.,-0.707106781186548,0.707106781186548));
#5539=DIRECTION('',(0.,1.,0.));
#5540=DIRECTION('',(0.,-0.707106781186548,-0.707106781186548));
#5541=DIRECTION('',(0.,0.,1.));
#5542=DIRECTION('center_axis',(0.,-1.,0.));
#5543=DIRECTION('ref_axis',(1.,0.,0.));
#5544=DIRECTION('',(-1.,0.,0.));
#5545=DIRECTION('center_axis',(0.,-0.707106781186548,-0.707106781186548));
#5546=DIRECTION('ref_axis',(-1.,0.,0.));
#5547=DIRECTION('',(1.,0.,0.));
#5548=DIRECTION('center_axis',(0.,0.707106781186548,0.707106781186548));
#5549=DIRECTION('ref_axis',(0.,0.707106781186547,-0.707106781186547));
#5550=DIRECTION('',(1.,0.,0.));
#5551=DIRECTION('center_axis',(0.,0.,1.));
#5552=DIRECTION('ref_axis',(1.,0.,0.));
#5553=DIRECTION('center_axis',(0.,0.,-1.));
#5554=DIRECTION('ref_axis',(1.,0.,0.));
#5555=DIRECTION('',(0.,0.,1.));
#5556=DIRECTION('center_axis',(0.,0.,-1.));
#5557=DIRECTION('ref_axis',(1.,0.,0.));
#5558=DIRECTION('center_axis',(0.,-0.707106781186548,0.707106781186548));
#5559=DIRECTION('ref_axis',(0.,0.707106781186547,0.707106781186547));
#5560=DIRECTION('center_axis',(0.,0.,-1.));
#5561=DIRECTION('ref_axis',(1.,0.,0.));
#5562=DIRECTION('center_axis',(0.,0.,1.));
#5563=DIRECTION('ref_axis',(1.,0.,0.));
#5564=DIRECTION('',(-1.,0.,0.));
#5565=DIRECTION('center_axis',(0.,0.,1.));
#5566=DIRECTION('ref_axis',(1.,0.,0.));
#5567=DIRECTION('',(-1.,0.,0.));
#5568=DIRECTION('center_axis',(0.,0.707106781186548,-0.707106781186548));
#5569=DIRECTION('ref_axis',(-1.,0.,0.));
#5570=DIRECTION('',(1.,0.,0.));
#5571=DIRECTION('center_axis',(0.,1.,0.));
#5572=DIRECTION('ref_axis',(-1.,0.,0.));
#6829=CARTESIAN_POINT('',(0.,0.,0.));
#6830=CARTESIAN_POINT('Origin',(0.,0.395,0.25));
#6831=CARTESIAN_POINT('',(-0.5,0.3,0.25));
#6832=CARTESIAN_POINT('',(0.5,0.3,0.25));
#6833=CARTESIAN_POINT('',(0.25,0.3,0.25));
#6834=CARTESIAN_POINT('',(-0.5,0.5,0.25));
#6835=CARTESIAN_POINT('',(-0.5,0.5,0.25));
#6836=CARTESIAN_POINT('',(0.5,0.5,0.25));
#6837=CARTESIAN_POINT('',(0.5,0.5,0.25));
#6838=CARTESIAN_POINT('',(0.5,0.29,0.25));
#6839=CARTESIAN_POINT('Origin',(0.5,0.5,0.25));
#6840=CARTESIAN_POINT('',(-0.5,0.5,0.4));
#6841=CARTESIAN_POINT('',(-0.5,0.5,0.25));
#6842=CARTESIAN_POINT('',(0.5,0.5,0.4));
#6843=CARTESIAN_POINT('',(0.5,0.5,0.4));
#6844=CARTESIAN_POINT('',(0.5,0.5,0.25));
#6845=CARTESIAN_POINT('Origin',(0.,0.,0.4));
#6846=CARTESIAN_POINT('',(-0.5,-0.5,0.4));
#6847=CARTESIAN_POINT('',(-0.5,0.5,0.4));
#6848=CARTESIAN_POINT('',(0.5,-0.5,0.4));
#6849=CARTESIAN_POINT('',(-0.5,-0.5,0.4));
#6850=CARTESIAN_POINT('',(0.5,-0.3,0.4));
#6851=CARTESIAN_POINT('',(-0.2117,2.59257727379495E-17,0.4));
#6852=CARTESIAN_POINT('Origin',(0.,0.,0.4));
#6853=CARTESIAN_POINT('Origin',(-0.5,0.3,0.));
#6854=CARTESIAN_POINT('',(-0.5,0.3,0.15));
#6855=CARTESIAN_POINT('',(-0.5,0.3,0.));
#6856=CARTESIAN_POINT('',(-0.5,0.15,0.));
#6857=CARTESIAN_POINT('',(-0.5,0.225,0.075));
#6858=CARTESIAN_POINT('',(-0.5,-0.15,0.));
#6859=CARTESIAN_POINT('',(-0.5,0.3,0.));
#6860=CARTESIAN_POINT('',(-0.5,-0.3,0.15));
#6861=CARTESIAN_POINT('',(-0.5,-0.075,-0.075));
#6862=CARTESIAN_POINT('',(-0.5,-0.3,0.25));
#6863=CARTESIAN_POINT('',(-0.5,-0.3,0.));
#6864=CARTESIAN_POINT('',(-0.5,-0.5,0.25));
#6865=CARTESIAN_POINT('',(-0.5,-0.29,0.25));
#6866=CARTESIAN_POINT('',(-0.5,-0.5,0.25));
#6867=CARTESIAN_POINT('Origin',(-0.5,-0.5,0.25));
#6868=CARTESIAN_POINT('',(0.5,-0.5,0.25));
#6869=CARTESIAN_POINT('',(-0.5,-0.5,0.25));
#6870=CARTESIAN_POINT('',(0.5,-0.5,0.25));
#6871=CARTESIAN_POINT('Origin',(0.,-0.395,0.25));
#6872=CARTESIAN_POINT('',(0.5,-0.3,0.25));
#6873=CARTESIAN_POINT('',(-0.25,-0.3,0.25));
#6874=CARTESIAN_POINT('',(0.5,-0.5,0.25));
#6875=CARTESIAN_POINT('Origin',(0.5,-0.3,0.));
#6876=CARTESIAN_POINT('',(0.5,-0.3,0.15));
#6877=CARTESIAN_POINT('',(0.5,-0.3,0.));
#6878=CARTESIAN_POINT('',(0.5,-0.15,0.));
#6879=CARTESIAN_POINT('',(0.5,-0.225,0.075));
#6880=CARTESIAN_POINT('',(0.5,0.15,0.));
#6881=CARTESIAN_POINT('',(0.5,-0.3,0.));
#6882=CARTESIAN_POINT('',(0.5,0.3,0.15));
#6883=CARTESIAN_POINT('',(0.5,0.075,-0.075));
#6884=CARTESIAN_POINT('',(0.5,0.3,0.));
#6885=CARTESIAN_POINT('Origin',(-0.5,-0.3,0.));
#6886=CARTESIAN_POINT('',(-0.25,-0.3,0.15));
#6887=CARTESIAN_POINT('Origin',(-0.25,-0.225,0.075));
#6888=CARTESIAN_POINT('',(-0.149388386429468,-0.15,0.));
#6889=CARTESIAN_POINT('',(-0.25,-0.15,0.));
#6890=CARTESIAN_POINT('',(0.149388386429468,-0.15,0.));
#6891=CARTESIAN_POINT('Origin',(0.,0.,-0.15));
#6892=CARTESIAN_POINT('',(-0.25,-0.15,0.));
#6893=CARTESIAN_POINT('Origin',(0.,0.,-0.1));
#6894=CARTESIAN_POINT('',(-0.2117,-2.59257727379495E-17,0.));
#6895=CARTESIAN_POINT('Origin',(0.,0.,0.));
#6896=CARTESIAN_POINT('',(-0.2117,-2.59257727379495E-17,-0.1));
#6897=CARTESIAN_POINT('',(-0.149388386429468,0.15,0.));
#6898=CARTESIAN_POINT('Origin',(0.,0.,0.));
#6899=CARTESIAN_POINT('',(0.149388386429468,0.15,0.));
#6900=CARTESIAN_POINT('Origin',(0.,0.,-0.15));
#6901=CARTESIAN_POINT('Origin',(0.,0.,0.));
#6902=CARTESIAN_POINT('Origin',(0.,0.,0.));
#6903=CARTESIAN_POINT('',(0.25,0.15,0.));
#6904=CARTESIAN_POINT('Origin',(0.,0.,0.));
#6905=CARTESIAN_POINT('',(0.25,0.15,0.));
#6906=CARTESIAN_POINT('Origin',(0.25,0.225,0.075));
#6907=CARTESIAN_POINT('',(0.25,0.3,0.15));
#6908=CARTESIAN_POINT('Origin',(0.5,0.3,0.));
#7767=UNCERTAINTY_MEASURE_WITH_UNIT(LENGTH_MEASURE(0.001),#7807,
'DISTANCE_ACCURACY_VALUE',
'Maximum model space distance between geometric entities at asserted c
onnectivities');
#7782=UNCERTAINTY_MEASURE_WITH_UNIT(LENGTH_MEASURE(0.001),#7807,
'DISTANCE_ACCURACY_VALUE',
'Maximum model space distance between geometric entities at asserted c
onnectivities');
#7791=(
GEOMETRIC_REPRESENTATION_CONTEXT(3)
GLOBAL_UNCERTAINTY_ASSIGNED_CONTEXT((#7767))
GLOBAL_UNIT_ASSIGNED_CONTEXT((#7807,#7809,#7810))
REPRESENTATION_CONTEXT('','3D')
);
#7806=(
GEOMETRIC_REPRESENTATION_CONTEXT(3)
GLOBAL_UNCERTAINTY_ASSIGNED_CONTEXT((#7782))
GLOBAL_UNIT_ASSIGNED_CONTEXT((#7807,#7809,#7810))
REPRESENTATION_CONTEXT('','3D')
);
#7807=(
LENGTH_UNIT()
NAMED_UNIT(*)
SI_UNIT(.CENTI.,.METRE.)
);
#7809=(
NAMED_UNIT(*)
PLANE_ANGLE_UNIT()
SI_UNIT($,.RADIAN.)
);
#7810=(
NAMED_UNIT(*)
SI_UNIT($,.STERADIAN.)
SOLID_ANGLE_UNIT()
);
#7819=SHAPE_DEFINITION_REPRESENTATION(#7842,#7918);
#7842=PRODUCT_DEFINITION_SHAPE('',$,#7942);
#7918=SHAPE_REPRESENTATION('',(#4597),#7791);
#7933=PRODUCT_DEFINITION_CONTEXT('part definition',#8004,'design');
#7942=PRODUCT_DEFINITION('Slot nut','Slot nut',#7965,#7933);
#7965=PRODUCT_DEFINITION_FORMATION('',$,#8014);
#8004=APPLICATION_CONTEXT(
'Core Data for Automotive Mechanical Design Process');
#8005=PRODUCT_CONTEXT('part definition',#8004,'mechanical');
#8014=PRODUCT('Slot nut','Slot nut','Slot nut',(#8005));
#8092=COLOUR_RGB('Black',0.12,0.14,0.17);
#8093=FILL_AREA_STYLE_COLOUR('',#8092);
#8094=FILL_AREA_STYLE('',(#8093));
#8095=SURFACE_STYLE_FILL_AREA(#8094);
#8096=SURFACE_SIDE_STYLE('',(#8095));
#8097=SURFACE_STYLE_USAGE(.BOTH.,#8096);
#8098=PRESENTATION_STYLE_ASSIGNMENT((#8097));
ENDSEC;
END-ISO-10303-21;
